ISO-10303-21;
HEADER;
/* Generated by software containing ST-Developer
 * from STEP Tools, Inc. (www.steptools.com) 
 */

FILE_DESCRIPTION(
/* description */ ('Bin tilter linkage'),
/* implementation_level */ '2;1');

FILE_NAME(
/* name */ 'Pivot spacer 5 mm (2).step',
/* time_stamp */ '2026-10-28T03:26:24-07:00',
/* author */ (''),
/* organization */ (''),
/* preprocessor_version */ 'ST-DEVELOPER v20.2',
/* originating_system */ 'Autodesk Translation Framework v15.17.0.0',
/* authorisation */ '');

FILE_SCHEMA (('AUTOMOTIVE_DESIGN { 1 0 10303 214 3 1 1 }'));
ENDSEC;

DATA;
#10=MECHANICAL_DESIGN_GEOMETRIC_PRESENTATION_REPRESENTATION('',(#953),#23728);
#733=SHAPE_REPRESENTATION_RELATIONSHIP('SRR','None',#24201,#839);
#839=ADVANCED_BREP_SHAPE_REPRESENTATION('',(#1066),#23701);
#953=STYLED_ITEM('',(#24779),#1066);
#1066=MANIFOLD_SOLID_BREP('Body1',#12484);
#1424=FACE_BOUND('',#3619,.T.);
#1425=FACE_BOUND('',#3621,.T.);
#1790=PLANE('',#15064);
#1791=PLANE('',#15065);
#2502=FACE_OUTER_BOUND('',#3616,.T.);
#2503=FACE_OUTER_BOUND('',#3617,.T.);
#2504=FACE_OUTER_BOUND('',#3618,.T.);
#2505=FACE_OUTER_BOUND('',#3620,.T.);
#3616=EDGE_LOOP('',(#10663,#10664,#10665,#10666));
#3617=EDGE_LOOP('',(#10667,#10668,#10669,#10670));
#3618=EDGE_LOOP('',(#10671));
#3619=EDGE_LOOP('',(#10672));
#3620=EDGE_LOOP('',(#10673));
#3621=EDGE_LOOP('',(#10674));
#4351=LINE('',#22711,#5026);
#4352=LINE('',#22717,#5027);
#5026=VECTOR('',#18744,0.605);
#5027=VECTOR('',#18751,0.800000000000001);
#5828=CIRCLE('',#15059,0.605);
#5829=CIRCLE('',#15060,0.605);
#5830=CIRCLE('',#15062,0.800000000000001);
#5831=CIRCLE('',#15063,0.800000000000001);
#6727=VERTEX_POINT('',#22708);
#6728=VERTEX_POINT('',#22710);
#6729=VERTEX_POINT('',#22714);
#6730=VERTEX_POINT('',#22716);
#8071=EDGE_CURVE('',#6727,#6727,#5828,.T.);
#8072=EDGE_CURVE('',#6727,#6728,#4351,.T.);
#8073=EDGE_CURVE('',#6728,#6728,#5829,.T.);
#8074=EDGE_CURVE('',#6729,#6729,#5830,.T.);
#8075=EDGE_CURVE('',#6729,#6730,#4352,.T.);
#8076=EDGE_CURVE('',#6730,#6730,#5831,.T.);
#10663=ORIENTED_EDGE('',*,*,#8071,.F.);
#10664=ORIENTED_EDGE('',*,*,#8072,.T.);
#10665=ORIENTED_EDGE('',*,*,#8073,.T.);
#10666=ORIENTED_EDGE('',*,*,#8072,.F.);
#10667=ORIENTED_EDGE('',*,*,#8074,.F.);
#10668=ORIENTED_EDGE('',*,*,#8075,.T.);
#10669=ORIENTED_EDGE('',*,*,#8076,.T.);
#10670=ORIENTED_EDGE('',*,*,#8075,.F.);
#10671=ORIENTED_EDGE('',*,*,#8074,.T.);
#10672=ORIENTED_EDGE('',*,*,#8071,.T.);
#10673=ORIENTED_EDGE('',*,*,#8076,.F.);
#10674=ORIENTED_EDGE('',*,*,#8073,.F.);
#11557=CYLINDRICAL_SURFACE('',#15058,0.605);
#11558=CYLINDRICAL_SURFACE('',#15061,0.800000000000001);
#12227=ADVANCED_FACE('',(#2502),#11557,.F.);
#12228=ADVANCED_FACE('',(#2503),#11558,.T.);
#12229=ADVANCED_FACE('',(#2504,#1424),#1790,.T.);
#12230=ADVANCED_FACE('',(#2505,#1425),#1791,.F.);
#12484=CLOSED_SHELL('',(#12227,#12228,#12229,#12230));
#15057=AXIS2_PLACEMENT_3D('',#22706,#18738,#18739);
#15058=AXIS2_PLACEMENT_3D('',#22707,#18740,#18741);
#15059=AXIS2_PLACEMENT_3D('',#22709,#18742,#18743);
#15060=AXIS2_PLACEMENT_3D('',#22712,#18745,#18746);
#15061=AXIS2_PLACEMENT_3D('',#22713,#18747,#18748);
#15062=AXIS2_PLACEMENT_3D('',#22715,#18749,#18750);
#15063=AXIS2_PLACEMENT_3D('',#22718,#18752,#18753);
#15064=AXIS2_PLACEMENT_3D('',#22719,#18754,#18755);
#15065=AXIS2_PLACEMENT_3D('',#22720,#18756,#18757);
#18738=DIRECTION('axis',(0.,0.,1.));
#18739=DIRECTION('refdir',(1.,0.,0.));
#18740=DIRECTION('center_axis',(0.,1.,0.));
#18741=DIRECTION('ref_axis',(1.,0.,0.));
#18742=DIRECTION('center_axis',(0.,-1.,0.));
#18743=DIRECTION('ref_axis',(1.,0.,0.));
#18744=DIRECTION('',(0.,-1.,0.));
#18745=DIRECTION('center_axis',(0.,-1.,0.));
#18746=DIRECTION('ref_axis',(1.,0.,0.));
#18747=DIRECTION('center_axis',(0.,1.,0.));
#18748=DIRECTION('ref_axis',(1.,0.,0.));
#18749=DIRECTION('center_axis',(0.,1.,0.));
#18750=DIRECTION('ref_axis',(1.,0.,0.));
#18751=DIRECTION('',(0.,-1.,0.));
#18752=DIRECTION('center_axis',(0.,1.,0.));
#18753=DIRECTION('ref_axis',(1.,0.,0.));
#18754=DIRECTION('center_axis',(0.,1.,0.));
#18755=DIRECTION('ref_axis',(1.,0.,0.));
#18756=DIRECTION('center_axis',(0.,1.,0.));
#18757=DIRECTION('ref_axis',(1.,0.,0.));
#22706=CARTESIAN_POINT('',(0.,0.,0.));
#22707=CARTESIAN_POINT('Origin',(9.39692620785909,-5.5,18.4202014332567));
#22708=CARTESIAN_POINT('',(8.79192620785908,-5.,18.4202014332567));
#22709=CARTESIAN_POINT('Origin',(9.39692620785909,-5.,18.4202014332567));
#22710=CARTESIAN_POINT('',(8.79192620785908,-5.5,18.4202014332567));
#22711=CARTESIAN_POINT('',(8.79192620785908,-5.5,18.4202014332567));
#22712=CARTESIAN_POINT('Origin',(9.39692620785909,-5.5,18.4202014332567));
#22713=CARTESIAN_POINT('Origin',(9.39692620785909,-5.5,18.4202014332567));
#22714=CARTESIAN_POINT('',(8.59692620785908,-5.,18.4202014332567));
#22715=CARTESIAN_POINT('Origin',(9.39692620785909,-5.,18.4202014332567));
#22716=CARTESIAN_POINT('',(8.59692620785908,-5.5,18.4202014332567));
#22717=CARTESIAN_POINT('',(8.59692620785908,-5.5,18.4202014332567));
#22718=CARTESIAN_POINT('Origin',(9.39692620785909,-5.5,18.4202014332567));
#22719=CARTESIAN_POINT('Origin',(9.39692620785909,-5.,18.4202014332567));
#22720=CARTESIAN_POINT('Origin',(9.39692620785909,-5.5,18.4202014332567));
#23584=UNCERTAINTY_MEASURE_WITH_UNIT(LENGTH_MEASURE(0.001),#23729,
'DISTANCE_ACCURACY_VALUE',
'Maximum model space distance between geometric entities at asserted c
onnectivities');
#23611=UNCERTAINTY_MEASURE_WITH_UNIT(LENGTH_MEASURE(0.001),#23729,
'DISTANCE_ACCURACY_VALUE',
'Maximum model space distance between geometric entities at asserted c
onnectivities');
#23701=(
GEOMETRIC_REPRESENTATION_CONTEXT(3)
GLOBAL_UNCERTAINTY_ASSIGNED_CONTEXT((#23584))
GLOBAL_UNIT_ASSIGNED_CONTEXT((#23729,#23731,#23732))
REPRESENTATION_CONTEXT('','3D')
);
#23728=(
GEOMETRIC_REPRESENTATION_CONTEXT(3)
GLOBAL_UNCERTAINTY_ASSIGNED_CONTEXT((#23611))
GLOBAL_UNIT_ASSIGNED_CONTEXT((#23729,#23731,#23732))
REPRESENTATION_CONTEXT('','3D')
);
#23729=(
LENGTH_UNIT()
NAMED_UNIT(*)
SI_UNIT(.CENTI.,.METRE.)
);
#23731=(
NAMED_UNIT(*)
PLANE_ANGLE_UNIT()
SI_UNIT($,.RADIAN.)
);
#23732=(
NAMED_UNIT(*)
SI_UNIT($,.STERADIAN.)
SOLID_ANGLE_UNIT()
);
#23822=SHAPE_DEFINITION_REPRESENTATION(#23989,#24201);
#23989=PRODUCT_DEFINITION_SHAPE('',$,#24318);
#24201=SHAPE_REPRESENTATION('',(#15057),#23701);
#24228=PRODUCT_DEFINITION_CONTEXT('part definition',#24578,'design');
#24318=PRODUCT_DEFINITION('Pivot spacer 5 mm (2)','Pivot spacer 5 mm (2)',
#24434,#24228);
#24434=PRODUCT_DEFINITION_FORMATION('',$,#24669);
#24578=APPLICATION_CONTEXT(
'Core Data for Automotive Mechanical Design Process');
#24579=PRODUCT_CONTEXT('part definition',#24578,'mechanical');
#24669=PRODUCT('Pivot spacer 5 mm (2)','Pivot spacer 5 mm (2)',
'Pivot spacer 5 mm (2)',(#24579));
#24773=COLOUR_RGB('Off White',0.89,0.88,0.83);
#24774=FILL_AREA_STYLE_COLOUR('',#24773);
#24775=FILL_AREA_STYLE('',(#24774));
#24776=SURFACE_STYLE_FILL_AREA(#24775);
#24777=SURFACE_SIDE_STYLE('',(#24776));
#24778=SURFACE_STYLE_USAGE(.BOTH.,#24777);
#24779=PRESENTATION_STYLE_ASSIGNMENT((#24778));
ENDSEC;
END-ISO-10303-21;
